ISO-10303-21;
HEADER;
/* Generated by software containing ST-Developer
 * from STEP Tools, Inc. (www.steptools.com) 
 */

FILE_DESCRIPTION(
/* description */ ('Bin tilter linkage'),
/* implementation_level */ '2;1');

FILE_NAME(
/* name */ 'Screw keeper fastener (1).step',
/* time_stamp */ '2026-10-28T03:26:24-07:00',
/* author */ (''),
/* organization */ (''),
/* preprocessor_version */ 'ST-DEVELOPER v20.2',
/* originating_system */ 'Autodesk Translation Framework v15.17.0.0',
/* authorisation */ '');

FILE_SCHEMA (('AUTOMOTIVE_DESIGN { 1 0 10303 214 3 1 1 }'));
ENDSEC;

DATA;
#10=MECHANICAL_DESIGN_GEOMETRIC_PRESENTATION_REPRESENTATION('',(#878),#23728);
#666=SHAPE_REPRESENTATION_RELATIONSHIP('SRR','None',#24130,#772);
#772=ADVANCED_BREP_SHAPE_REPRESENTATION('',(#992),#23630);
#878=STYLED_ITEM('',(#24772),#992);
#992=MANIFOLD_SOLID_BREP('Body1',#12408);
#1194=FACE_BOUND('',#2921,.T.);
#1566=PLANE('',#13985);
#1567=PLANE('',#13990);
#1568=PLANE('',#13993);
#2036=FACE_OUTER_BOUND('',#2920,.T.);
#2037=FACE_OUTER_BOUND('',#2922,.T.);
#2038=FACE_OUTER_BOUND('',#2923,.T.);
#2039=FACE_OUTER_BOUND('',#2924,.T.);
#2040=FACE_OUTER_BOUND('',#2925,.T.);
#2920=EDGE_LOOP('',(#9003));
#2921=EDGE_LOOP('',(#9004));
#2922=EDGE_LOOP('',(#9005,#9006,#9007,#9008));
#2923=EDGE_LOOP('',(#9009));
#2924=EDGE_LOOP('',(#9010,#9011,#9012,#9013));
#2925=EDGE_LOOP('',(#9014));
#4020=LINE('',#20442,#4695);
#4021=LINE('',#20448,#4696);
#4695=VECTOR('',#16271,0.35);
#4696=VECTOR('',#16280,0.2);
#5343=CIRCLE('',#13986,0.35);
#5344=CIRCLE('',#13987,0.2);
#5345=CIRCLE('',#13989,0.35);
#5346=CIRCLE('',#13992,0.2);
#6167=VERTEX_POINT('',#20436);
#6168=VERTEX_POINT('',#20438);
#6169=VERTEX_POINT('',#20441);
#6170=VERTEX_POINT('',#20446);
#7241=EDGE_CURVE('',#6167,#6167,#5343,.T.);
#7242=EDGE_CURVE('',#6168,#6168,#5344,.T.);
#7243=EDGE_CURVE('',#6167,#6169,#4020,.T.);
#7244=EDGE_CURVE('',#6169,#6169,#5345,.T.);
#7245=EDGE_CURVE('',#6170,#6170,#5346,.T.);
#7246=EDGE_CURVE('',#6170,#6168,#4021,.T.);
#9003=ORIENTED_EDGE('',*,*,#7241,.T.);
#9004=ORIENTED_EDGE('',*,*,#7242,.F.);
#9005=ORIENTED_EDGE('',*,*,#7241,.F.);
#9006=ORIENTED_EDGE('',*,*,#7243,.T.);
#9007=ORIENTED_EDGE('',*,*,#7244,.T.);
#9008=ORIENTED_EDGE('',*,*,#7243,.F.);
#9009=ORIENTED_EDGE('',*,*,#7244,.F.);
#9010=ORIENTED_EDGE('',*,*,#7245,.F.);
#9011=ORIENTED_EDGE('',*,*,#7246,.T.);
#9012=ORIENTED_EDGE('',*,*,#7242,.T.);
#9013=ORIENTED_EDGE('',*,*,#7246,.F.);
#9014=ORIENTED_EDGE('',*,*,#7245,.T.);
#11339=CYLINDRICAL_SURFACE('',#13988,0.35);
#11340=CYLINDRICAL_SURFACE('',#13991,0.2);
#11761=ADVANCED_FACE('',(#2036,#1194),#1566,.T.);
#11762=ADVANCED_FACE('',(#2037),#11339,.T.);
#11763=ADVANCED_FACE('',(#2038),#1567,.F.);
#11764=ADVANCED_FACE('',(#2039),#11340,.T.);
#11765=ADVANCED_FACE('',(#2040),#1568,.T.);
#12408=CLOSED_SHELL('',(#11761,#11762,#11763,#11764,#11765));
#13984=AXIS2_PLACEMENT_3D('',#20434,#16261,#16262);
#13985=AXIS2_PLACEMENT_3D('',#20435,#16263,#16264);
#13986=AXIS2_PLACEMENT_3D('',#20437,#16265,#16266);
#13987=AXIS2_PLACEMENT_3D('',#20439,#16267,#16268);
#13988=AXIS2_PLACEMENT_3D('',#20440,#16269,#16270);
#13989=AXIS2_PLACEMENT_3D('',#20443,#16272,#16273);
#13990=AXIS2_PLACEMENT_3D('',#20444,#16274,#16275);
#13991=AXIS2_PLACEMENT_3D('',#20445,#16276,#16277);
#13992=AXIS2_PLACEMENT_3D('',#20447,#16278,#16279);
#13993=AXIS2_PLACEMENT_3D('',#20449,#16281,#16282);
#16261=DIRECTION('axis',(0.,0.,1.));
#16262=DIRECTION('refdir',(1.,0.,0.));
#16263=DIRECTION('center_axis',(1.,0.,0.));
#16264=DIRECTION('ref_axis',(0.,0.,-1.));
#16265=DIRECTION('center_axis',(1.,0.,0.));
#16266=DIRECTION('ref_axis',(0.,0.,-1.));
#16267=DIRECTION('center_axis',(1.,0.,0.));
#16268=DIRECTION('ref_axis',(0.,0.,-1.));
#16269=DIRECTION('center_axis',(1.,0.,0.));
#16270=DIRECTION('ref_axis',(0.,0.,-1.));
#16271=DIRECTION('',(-1.,0.,0.));
#16272=DIRECTION('center_axis',(1.,0.,0.));
#16273=DIRECTION('ref_axis',(0.,0.,-1.));
#16274=DIRECTION('center_axis',(1.,0.,0.));
#16275=DIRECTION('ref_axis',(0.,0.,-1.));
#16276=DIRECTION('center_axis',(1.,0.,0.));
#16277=DIRECTION('ref_axis',(0.,0.,-1.));
#16278=DIRECTION('center_axis',(1.,0.,0.));
#16279=DIRECTION('ref_axis',(0.,0.,-1.));
#16280=DIRECTION('',(-1.,0.,0.));
#16281=DIRECTION('center_axis',(1.,0.,0.));
#16282=DIRECTION('ref_axis',(0.,0.,-1.));
#20434=CARTESIAN_POINT('',(0.,0.,0.));
#20435=CARTESIAN_POINT('Origin',(-10.2,-4.5,6.15));
#20436=CARTESIAN_POINT('',(-10.2,-4.5,6.5));
#20437=CARTESIAN_POINT('Origin',(-10.2,-4.5,6.15));
#20438=CARTESIAN_POINT('',(-10.2,-4.5,6.35));
#20439=CARTESIAN_POINT('Origin',(-10.2,-4.5,6.15));
#20440=CARTESIAN_POINT('Origin',(-10.6,-4.5,6.15));
#20441=CARTESIAN_POINT('',(-10.6,-4.5,6.5));
#20442=CARTESIAN_POINT('',(-10.6,-4.5,6.5));
#20443=CARTESIAN_POINT('Origin',(-10.6,-4.5,6.15));
#20444=CARTESIAN_POINT('Origin',(-10.6,-4.5,6.15));
#20445=CARTESIAN_POINT('Origin',(-10.2,-4.5,6.15));
#20446=CARTESIAN_POINT('',(-9.5,-4.5,6.35));
#20447=CARTESIAN_POINT('Origin',(-9.5,-4.5,6.15));
#20448=CARTESIAN_POINT('',(-10.2,-4.5,6.35));
#20449=CARTESIAN_POINT('Origin',(-9.5,-4.5,6.15));
#23513=UNCERTAINTY_MEASURE_WITH_UNIT(LENGTH_MEASURE(0.001),#23729,
'DISTANCE_ACCURACY_VALUE',
'Maximum model space distance between geometric entities at asserted c
onnectivities');
#23611=UNCERTAINTY_MEASURE_WITH_UNIT(LENGTH_MEASURE(0.001),#23729,
'DISTANCE_ACCURACY_VALUE',
'Maximum model space distance between geometric entities at asserted c
onnectivities');
#23630=(
GEOMETRIC_REPRESENTATION_CONTEXT(3)
GLOBAL_UNCERTAINTY_ASSIGNED_CONTEXT((#23513))
GLOBAL_UNIT_ASSIGNED_CONTEXT((#23729,#23731,#23732))
REPRESENTATION_CONTEXT('','3D')
);
#23728=(
GEOMETRIC_REPRESENTATION_CONTEXT(3)
GLOBAL_UNCERTAINTY_ASSIGNED_CONTEXT((#23611))
GLOBAL_UNIT_ASSIGNED_CONTEXT((#23729,#23731,#23732))
REPRESENTATION_CONTEXT('','3D')
);
#23729=(
LENGTH_UNIT()
NAMED_UNIT(*)
SI_UNIT(.CENTI.,.METRE.)
);
#23731=(
NAMED_UNIT(*)
PLANE_ANGLE_UNIT()
SI_UNIT($,.RADIAN.)
);
#23732=(
NAMED_UNIT(*)
SI_UNIT($,.STERADIAN.)
SOLID_ANGLE_UNIT()
);
#23751=SHAPE_DEFINITION_REPRESENTATION(#23867,#24130);
#23867=PRODUCT_DEFINITION_SHAPE('',$,#24247);
#24130=SHAPE_REPRESENTATION('',(#13984),#23630);
#24228=PRODUCT_DEFINITION_CONTEXT('part definition',#24578,'design');
#24247=PRODUCT_DEFINITION('Screw keeper fastener (1)',
'Screw keeper fastener (1)',#24363,#24228);
#24363=PRODUCT_DEFINITION_FORMATION('',$,#24598);
#24578=APPLICATION_CONTEXT(
'Core Data for Automotive Mechanical Design Process');
#24579=PRODUCT_CONTEXT('part definition',#24578,'mechanical');
#24598=PRODUCT('Screw keeper fastener (1)','Screw keeper fastener (1)',
'Screw keeper fastener (1)',(#24579));
#24766=COLOUR_RGB('Black',0.12,0.14,0.17);
#24767=FILL_AREA_STYLE_COLOUR('',#24766);
#24768=FILL_AREA_STYLE('',(#24767));
#24769=SURFACE_STYLE_FILL_AREA(#24768);
#24770=SURFACE_SIDE_STYLE('',(#24769));
#24771=SURFACE_STYLE_USAGE(.BOTH.,#24770);
#24772=PRESENTATION_STYLE_ASSIGNMENT((#24771));
ENDSEC;
END-ISO-10303-21;
